ISO-10303-21;
HEADER;
/* Generated by software containing ST-Developer
 * from STEP Tools, Inc. (www.steptools.com) 
 */

FILE_DESCRIPTION(
/* description */ ('Cam-driven reciprocating slide'),
/* implementation_level */ '2;1');

FILE_NAME(
/* name */ 'Foot (1).step',
/* time_stamp */ '2026-10-28T03:25:20-07:00',
/* author */ (''),
/* organization */ (''),
/* preprocessor_version */ 'ST-DEVELOPER v20.2',
/* originating_system */ 'Autodesk Translation Framework v15.17.0.0',
/* authorisation */ '');

FILE_SCHEMA (('AUTOMOTIVE_DESIGN { 1 0 10303 214 3 1 1 }'));
ENDSEC;

DATA;
#10=MECHANICAL_DESIGN_GEOMETRIC_PRESENTATION_REPRESENTATION('',(#424),#13277);
#350=SHAPE_REPRESENTATION_RELATIONSHIP('SRR','None',#13443,#387);
#387=ADVANCED_BREP_SHAPE_REPRESENTATION('',(#468),#13238);
#424=STYLED_ITEM('',(#13734),#468);
#468=MANIFOLD_SOLID_BREP('Body1',#6400);
#698=PLANE('',#6893);
#699=PLANE('',#6894);
#700=PLANE('',#6895);
#701=PLANE('',#6896);
#702=PLANE('',#6897);
#703=PLANE('',#6898);
#924=FACE_OUTER_BOUND('',#1316,.T.);
#925=FACE_OUTER_BOUND('',#1317,.T.);
#926=FACE_OUTER_BOUND('',#1318,.T.);
#927=FACE_OUTER_BOUND('',#1319,.T.);
#928=FACE_OUTER_BOUND('',#1320,.T.);
#929=FACE_OUTER_BOUND('',#1321,.T.);
#1316=EDGE_LOOP('',(#4444,#4445,#4446,#4447));
#1317=EDGE_LOOP('',(#4448,#4449,#4450,#4451));
#1318=EDGE_LOOP('',(#4452,#4453,#4454,#4455));
#1319=EDGE_LOOP('',(#4456,#4457,#4458,#4459));
#1320=EDGE_LOOP('',(#4460,#4461,#4462,#4463));
#1321=EDGE_LOOP('',(#4464,#4465,#4466,#4467));
#1875=LINE('',#9861,#2314);
#1876=LINE('',#9863,#2315);
#1877=LINE('',#9865,#2316);
#1878=LINE('',#9866,#2317);
#1879=LINE('',#9869,#2318);
#1880=LINE('',#9871,#2319);
#1881=LINE('',#9872,#2320);
#1882=LINE('',#9875,#2321);
#1883=LINE('',#9877,#2322);
#1884=LINE('',#9878,#2323);
#1885=LINE('',#9880,#2324);
#1886=LINE('',#9881,#2325);
#2314=VECTOR('',#7793,1.);
#2315=VECTOR('',#7794,1.);
#2316=VECTOR('',#7795,1.);
#2317=VECTOR('',#7796,1.);
#2318=VECTOR('',#7799,1.);
#2319=VECTOR('',#7800,1.);
#2320=VECTOR('',#7801,1.);
#2321=VECTOR('',#7804,1.);
#2322=VECTOR('',#7805,1.);
#2323=VECTOR('',#7806,1.);
#2324=VECTOR('',#7809,1.);
#2325=VECTOR('',#7810,1.);
#3071=VERTEX_POINT('',#9859);
#3072=VERTEX_POINT('',#9860);
#3073=VERTEX_POINT('',#9862);
#3074=VERTEX_POINT('',#9864);
#3075=VERTEX_POINT('',#9868);
#3076=VERTEX_POINT('',#9870);
#3077=VERTEX_POINT('',#9874);
#3078=VERTEX_POINT('',#9876);
#3612=EDGE_CURVE('',#3071,#3072,#1875,.T.);
#3613=EDGE_CURVE('',#3072,#3073,#1876,.T.);
#3614=EDGE_CURVE('',#3074,#3073,#1877,.T.);
#3615=EDGE_CURVE('',#3071,#3074,#1878,.T.);
#3616=EDGE_CURVE('',#3075,#3071,#1879,.T.);
#3617=EDGE_CURVE('',#3076,#3074,#1880,.T.);
#3618=EDGE_CURVE('',#3075,#3076,#1881,.T.);
#3619=EDGE_CURVE('',#3077,#3075,#1882,.T.);
#3620=EDGE_CURVE('',#3078,#3076,#1883,.T.);
#3621=EDGE_CURVE('',#3077,#3078,#1884,.T.);
#3622=EDGE_CURVE('',#3072,#3077,#1885,.T.);
#3623=EDGE_CURVE('',#3073,#3078,#1886,.T.);
#4444=ORIENTED_EDGE('',*,*,#3612,.T.);
#4445=ORIENTED_EDGE('',*,*,#3613,.T.);
#4446=ORIENTED_EDGE('',*,*,#3614,.F.);
#4447=ORIENTED_EDGE('',*,*,#3615,.F.);
#4448=ORIENTED_EDGE('',*,*,#3616,.T.);
#4449=ORIENTED_EDGE('',*,*,#3615,.T.);
#4450=ORIENTED_EDGE('',*,*,#3617,.F.);
#4451=ORIENTED_EDGE('',*,*,#3618,.F.);
#4452=ORIENTED_EDGE('',*,*,#3619,.T.);
#4453=ORIENTED_EDGE('',*,*,#3618,.T.);
#4454=ORIENTED_EDGE('',*,*,#3620,.F.);
#4455=ORIENTED_EDGE('',*,*,#3621,.F.);
#4456=ORIENTED_EDGE('',*,*,#3622,.T.);
#4457=ORIENTED_EDGE('',*,*,#3621,.T.);
#4458=ORIENTED_EDGE('',*,*,#3623,.F.);
#4459=ORIENTED_EDGE('',*,*,#3613,.F.);
#4460=ORIENTED_EDGE('',*,*,#3623,.T.);
#4461=ORIENTED_EDGE('',*,*,#3620,.T.);
#4462=ORIENTED_EDGE('',*,*,#3617,.T.);
#4463=ORIENTED_EDGE('',*,*,#3614,.T.);
#4464=ORIENTED_EDGE('',*,*,#3622,.F.);
#4465=ORIENTED_EDGE('',*,*,#3612,.F.);
#4466=ORIENTED_EDGE('',*,*,#3616,.F.);
#4467=ORIENTED_EDGE('',*,*,#3619,.F.);
#6042=ADVANCED_FACE('',(#924),#698,.T.);
#6043=ADVANCED_FACE('',(#925),#699,.T.);
#6044=ADVANCED_FACE('',(#926),#700,.T.);
#6045=ADVANCED_FACE('',(#927),#701,.T.);
#6046=ADVANCED_FACE('',(#928),#702,.T.);
#6047=ADVANCED_FACE('',(#929),#703,.F.);
#6400=CLOSED_SHELL('',(#6042,#6043,#6044,#6045,#6046,#6047));
#6892=AXIS2_PLACEMENT_3D('',#9857,#7789,#7790);
#6893=AXIS2_PLACEMENT_3D('',#9858,#7791,#7792);
#6894=AXIS2_PLACEMENT_3D('',#9867,#7797,#7798);
#6895=AXIS2_PLACEMENT_3D('',#9873,#7802,#7803);
#6896=AXIS2_PLACEMENT_3D('',#9879,#7807,#7808);
#6897=AXIS2_PLACEMENT_3D('',#9882,#7811,#7812);
#6898=AXIS2_PLACEMENT_3D('',#9883,#7813,#7814);
#7789=DIRECTION('axis',(0.,0.,1.));
#7790=DIRECTION('refdir',(1.,0.,0.));
#7791=DIRECTION('center_axis',(0.,1.,0.));
#7792=DIRECTION('ref_axis',(-1.,0.,0.));
#7793=DIRECTION('',(-1.,0.,0.));
#7794=DIRECTION('',(0.,0.,1.));
#7795=DIRECTION('',(-1.,0.,0.));
#7796=DIRECTION('',(0.,0.,1.));
#7797=DIRECTION('center_axis',(1.,0.,0.));
#7798=DIRECTION('ref_axis',(0.,1.,0.));
#7799=DIRECTION('',(0.,1.,0.));
#7800=DIRECTION('',(0.,1.,0.));
#7801=DIRECTION('',(0.,0.,1.));
#7802=DIRECTION('center_axis',(0.,-1.,0.));
#7803=DIRECTION('ref_axis',(1.,0.,0.));
#7804=DIRECTION('',(1.,0.,0.));
#7805=DIRECTION('',(1.,0.,0.));
#7806=DIRECTION('',(0.,0.,1.));
#7807=DIRECTION('center_axis',(-1.,0.,0.));
#7808=DIRECTION('ref_axis',(0.,-1.,0.));
#7809=DIRECTION('',(0.,-1.,0.));
#7810=DIRECTION('',(0.,-1.,0.));
#7811=DIRECTION('center_axis',(0.,0.,1.));
#7812=DIRECTION('ref_axis',(1.,0.,0.));
#7813=DIRECTION('center_axis',(0.,0.,1.));
#7814=DIRECTION('ref_axis',(1.,0.,0.));
#9857=CARTESIAN_POINT('',(0.,0.,0.));
#9858=CARTESIAN_POINT('Origin',(6.,9.,-0.8));
#9859=CARTESIAN_POINT('',(6.,9.,-0.8));
#9860=CARTESIAN_POINT('',(5.,9.,-0.8));
#9861=CARTESIAN_POINT('',(6.,9.,-0.8));
#9862=CARTESIAN_POINT('',(5.,9.,0.));
#9863=CARTESIAN_POINT('',(5.,9.,-0.8));
#9864=CARTESIAN_POINT('',(6.,9.,0.));
#9865=CARTESIAN_POINT('',(6.,9.,0.));
#9866=CARTESIAN_POINT('',(6.,9.,-0.8));
#9867=CARTESIAN_POINT('Origin',(6.,-5.5,-0.8));
#9868=CARTESIAN_POINT('',(6.,-5.5,-0.8));
#9869=CARTESIAN_POINT('',(6.,-5.5,-0.8));
#9870=CARTESIAN_POINT('',(6.,-5.5,0.));
#9871=CARTESIAN_POINT('',(6.,-5.5,0.));
#9872=CARTESIAN_POINT('',(6.,-5.5,-0.8));
#9873=CARTESIAN_POINT('Origin',(5.,-5.5,-0.8));
#9874=CARTESIAN_POINT('',(5.,-5.5,-0.8));
#9875=CARTESIAN_POINT('',(5.,-5.5,-0.8));
#9876=CARTESIAN_POINT('',(5.,-5.5,0.));
#9877=CARTESIAN_POINT('',(5.,-5.5,0.));
#9878=CARTESIAN_POINT('',(5.,-5.5,-0.8));
#9879=CARTESIAN_POINT('Origin',(5.,9.,-0.8));
#9880=CARTESIAN_POINT('',(5.,9.,-0.8));
#9881=CARTESIAN_POINT('',(5.,9.,0.));
#9882=CARTESIAN_POINT('Origin',(5.5,1.75,0.));
#9883=CARTESIAN_POINT('Origin',(5.5,1.75,-0.8));
#13194=UNCERTAINTY_MEASURE_WITH_UNIT(LENGTH_MEASURE(0.001),#13278,
'DISTANCE_ACCURACY_VALUE',
'Maximum model space distance between geometric entities at asserted c
onnectivities');
#13233=UNCERTAINTY_MEASURE_WITH_UNIT(LENGTH_MEASURE(0.001),#13278,
'DISTANCE_ACCURACY_VALUE',
'Maximum model space distance between geometric entities at asserted c
onnectivities');
#13238=(
GEOMETRIC_REPRESENTATION_CONTEXT(3)
GLOBAL_UNCERTAINTY_ASSIGNED_CONTEXT((#13194))
GLOBAL_UNIT_ASSIGNED_CONTEXT((#13278,#13280,#13281))
REPRESENTATION_CONTEXT('','3D')
);
#13277=(
GEOMETRIC_REPRESENTATION_CONTEXT(3)
GLOBAL_UNCERTAINTY_ASSIGNED_CONTEXT((#13233))
GLOBAL_UNIT_ASSIGNED_CONTEXT((#13278,#13280,#13281))
REPRESENTATION_CONTEXT('','3D')
);
#13278=(
LENGTH_UNIT()
NAMED_UNIT(*)
SI_UNIT(.CENTI.,.METRE.)
);
#13280=(
NAMED_UNIT(*)
PLANE_ANGLE_UNIT()
SI_UNIT($,.RADIAN.)
);
#13281=(
NAMED_UNIT(*)
SI_UNIT($,.STERADIAN.)
SOLID_ANGLE_UNIT()
);
#13286=SHAPE_DEFINITION_REPRESENTATION(#13329,#13443);
#13329=PRODUCT_DEFINITION_SHAPE('',$,#13487);
#13443=SHAPE_REPRESENTATION('',(#6892),#13238);
#13482=PRODUCT_DEFINITION_CONTEXT('part definition',#13613,'design');
#13487=PRODUCT_DEFINITION('Foot (1)','Foot (1)',#13530,#13482);
#13530=PRODUCT_DEFINITION_FORMATION('',$,#13619);
#13613=APPLICATION_CONTEXT(
'Core Data for Automotive Mechanical Design Process');
#13614=PRODUCT_CONTEXT('part definition',#13613,'mechanical');
#13619=PRODUCT('Foot (1)','Foot (1)','Foot (1)',(#13614));
#13728=COLOUR_RGB('Off White',0.89,0.88,0.83);
#13729=FILL_AREA_STYLE_COLOUR('',#13728);
#13730=FILL_AREA_STYLE('',(#13729));
#13731=SURFACE_STYLE_FILL_AREA(#13730);
#13732=SURFACE_SIDE_STYLE('',(#13731));
#13733=SURFACE_STYLE_USAGE(.BOTH.,#13732);
#13734=PRESENTATION_STYLE_ASSIGNMENT((#13733));
ENDSEC;
END-ISO-10303-21;
